ISO-10303-21;
HEADER;
/* Generated by software containing ST-Developer
 * from STEP Tools, Inc. (www.steptools.com) 
 */

FILE_DESCRIPTION(
/* description */ ('Pallet stop with pneumatic fitting'),
/* implementation_level */ '2;1');

FILE_NAME(
/* name */ 'Cap Screw - M4x16.step',
/* time_stamp */ '2026-10-27T10:51:41-07:00',
/* author */ (''),
/* organization */ (''),
/* preprocessor_version */ 'ST-DEVELOPER v20.2',
/* originating_system */ 'Autodesk Translation Framework v15.17.0.0',
/* authorisation */ '');

FILE_SCHEMA (('AUTOMOTIVE_DESIGN { 1 0 10303 214 3 1 1 }'));
ENDSEC;

DATA;
#10=MECHANICAL_DESIGN_GEOMETRIC_PRESENTATION_REPRESENTATION('',(#388),#10265);
#24=ORIENTED_CLOSED_SHELL('',*,#5078,.F.);
#34=CONICAL_SURFACE('',#6010,0.325,0.785398163397448);
#35=CONICAL_SURFACE('',#6014,0.335,0.785398163397448);
#36=CONICAL_SURFACE('',#6018,0.21,0.463647609000806);
#37=CONICAL_SURFACE('',#6022,0.18,0.785398163397448);
#39=BREP_WITH_VOIDS('Body1',#5077,(#24));
#324=SHAPE_REPRESENTATION_RELATIONSHIP('SRR','None',#10440,#356);
#356=ADVANCED_BREP_SHAPE_REPRESENTATION('',(#39),#10264);
#388=STYLED_ITEM('',(#10662),#39);
#544=FACE_BOUND('',#1477,.T.);
#725=PLANE('',#6008);
#726=PLANE('',#6016);
#727=PLANE('',#6024);
#728=PLANE('',#6025);
#729=PLANE('',#6026);
#730=PLANE('',#6027);
#731=PLANE('',#6028);
#732=PLANE('',#6029);
#733=PLANE('',#6030);
#734=PLANE('',#6031);
#735=PLANE('',#6032);
#1033=FACE_OUTER_BOUND('',#1472,.T.);
#1034=FACE_OUTER_BOUND('',#1473,.T.);
#1035=FACE_OUTER_BOUND('',#1474,.T.);
#1036=FACE_OUTER_BOUND('',#1475,.T.);
#1037=FACE_OUTER_BOUND('',#1476,.T.);
#1038=FACE_OUTER_BOUND('',#1478,.T.);
#1039=FACE_OUTER_BOUND('',#1479,.T.);
#1040=FACE_OUTER_BOUND('',#1480,.T.);
#1041=FACE_OUTER_BOUND('',#1481,.T.);
#1042=FACE_OUTER_BOUND('',#1482,.T.);
#1043=FACE_OUTER_BOUND('',#1483,.T.);
#1044=FACE_OUTER_BOUND('',#1484,.T.);
#1045=FACE_OUTER_BOUND('',#1485,.T.);
#1046=FACE_OUTER_BOUND('',#1486,.T.);
#1047=FACE_OUTER_BOUND('',#1487,.T.);
#1048=FACE_OUTER_BOUND('',#1488,.T.);
#1049=FACE_OUTER_BOUND('',#1489,.T.);
#1472=EDGE_LOOP('',(#4558));
#1473=EDGE_LOOP('',(#4559,#4560,#4561,#4562));
#1474=EDGE_LOOP('',(#4563,#4564,#4565,#4566));
#1475=EDGE_LOOP('',(#4567,#4568,#4569,#4570));
#1476=EDGE_LOOP('',(#4571));
#1477=EDGE_LOOP('',(#4572));
#1478=EDGE_LOOP('',(#4573,#4574,#4575,#4576));
#1479=EDGE_LOOP('',(#4577,#4578,#4579,#4580));
#1480=EDGE_LOOP('',(#4581,#4582,#4583,#4584));
#1481=EDGE_LOOP('',(#4585));
#1482=EDGE_LOOP('',(#4586,#4587,#4588,#4589));
#1483=EDGE_LOOP('',(#4590,#4591,#4592,#4593));
#1484=EDGE_LOOP('',(#4594,#4595,#4596,#4597));
#1485=EDGE_LOOP('',(#4598,#4599,#4600,#4601));
#1486=EDGE_LOOP('',(#4602,#4603,#4604,#4605));
#1487=EDGE_LOOP('',(#4606,#4607,#4608,#4609));
#1488=EDGE_LOOP('',(#4610,#4611,#4612,#4613,#4614,#4615));
#1489=EDGE_LOOP('',(#4616,#4617,#4618,#4619,#4620,#4621));
#1801=LINE('',#10071,#2136);
#1802=LINE('',#10075,#2137);
#1803=LINE('',#10079,#2138);
#1804=LINE('',#10086,#2139);
#1805=LINE('',#10090,#2140);
#1806=LINE('',#10094,#2141);
#1807=LINE('',#10099,#2142);
#1808=LINE('',#10101,#2143);
#1809=LINE('',#10103,#2144);
#1810=LINE('',#10104,#2145);
#1811=LINE('',#10107,#2146);
#1812=LINE('',#10109,#2147);
#1813=LINE('',#10110,#2148);
#1814=LINE('',#10113,#2149);
#1815=LINE('',#10115,#2150);
#1816=LINE('',#10116,#2151);
#1817=LINE('',#10119,#2152);
#1818=LINE('',#10121,#2153);
#1819=LINE('',#10122,#2154);
#1820=LINE('',#10125,#2155);
#1821=LINE('',#10127,#2156);
#1822=LINE('',#10128,#2157);
#1823=LINE('',#10130,#2158);
#1824=LINE('',#10131,#2159);
#2136=VECTOR('',#7560,0.325);
#2137=VECTOR('',#7565,0.35);
#2138=VECTOR('',#7570,0.335);
#2139=VECTOR('',#7579,0.21);
#2140=VECTOR('',#7584,0.2);
#2141=VECTOR('',#7589,0.18);
#2142=VECTOR('',#7594,1.);
#2143=VECTOR('',#7595,1.);
#2144=VECTOR('',#7596,1.);
#2145=VECTOR('',#7597,1.);
#2146=VECTOR('',#7600,1.);
#2147=VECTOR('',#7601,1.);
#2148=VECTOR('',#7602,1.);
#2149=VECTOR('',#7605,1.);
#2150=VECTOR('',#7606,1.);
#2151=VECTOR('',#7607,1.);
#2152=VECTOR('',#7610,1.);
#2153=VECTOR('',#7611,1.);
#2154=VECTOR('',#7612,1.);
#2155=VECTOR('',#7615,1.);
#2156=VECTOR('',#7616,1.);
#2157=VECTOR('',#7617,1.);
#2158=VECTOR('',#7620,1.);
#2159=VECTOR('',#7621,1.);
#2399=CIRCLE('',#6009,0.3);
#2400=CIRCLE('',#6011,0.35);
#2401=CIRCLE('',#6013,0.35);
#2402=CIRCLE('',#6015,0.32);
#2403=CIRCLE('',#6017,0.22);
#2404=CIRCLE('',#6019,0.1954);
#2405=CIRCLE('',#6021,0.1954);
#2406=CIRCLE('',#6023,0.16);
#2784=VERTEX_POINT('',#10066);
#2785=VERTEX_POINT('',#10069);
#2786=VERTEX_POINT('',#10073);
#2787=VERTEX_POINT('',#10077);
#2788=VERTEX_POINT('',#10081);
#2789=VERTEX_POINT('',#10084);
#2790=VERTEX_POINT('',#10088);
#2791=VERTEX_POINT('',#10092);
#2792=VERTEX_POINT('',#10097);
#2793=VERTEX_POINT('',#10098);
#2794=VERTEX_POINT('',#10100);
#2795=VERTEX_POINT('',#10102);
#2796=VERTEX_POINT('',#10106);
#2797=VERTEX_POINT('',#10108);
#2798=VERTEX_POINT('',#10112);
#2799=VERTEX_POINT('',#10114);
#2800=VERTEX_POINT('',#10118);
#2801=VERTEX_POINT('',#10120);
#2802=VERTEX_POINT('',#10124);
#2803=VERTEX_POINT('',#10126);
#3378=EDGE_CURVE('',#2784,#2784,#2399,.T.);
#3379=EDGE_CURVE('',#2785,#2785,#2400,.T.);
#3380=EDGE_CURVE('',#2785,#2784,#1801,.T.);
#3381=EDGE_CURVE('',#2786,#2786,#2401,.T.);
#3382=EDGE_CURVE('',#2786,#2785,#1802,.T.);
#3383=EDGE_CURVE('',#2787,#2787,#2402,.T.);
#3384=EDGE_CURVE('',#2787,#2786,#1803,.T.);
#3385=EDGE_CURVE('',#2788,#2788,#2403,.T.);
#3386=EDGE_CURVE('',#2789,#2789,#2404,.F.);
#3387=EDGE_CURVE('',#2789,#2788,#1804,.T.);
#3388=EDGE_CURVE('',#2790,#2790,#2405,.F.);
#3389=EDGE_CURVE('',#2790,#2789,#1805,.T.);
#3390=EDGE_CURVE('',#2791,#2791,#2406,.T.);
#3391=EDGE_CURVE('',#2791,#2790,#1806,.T.);
#3392=EDGE_CURVE('',#2792,#2793,#1807,.T.);
#3393=EDGE_CURVE('',#2793,#2794,#1808,.T.);
#3394=EDGE_CURVE('',#2794,#2795,#1809,.T.);
#3395=EDGE_CURVE('',#2792,#2795,#1810,.T.);
#3396=EDGE_CURVE('',#2793,#2796,#1811,.T.);
#3397=EDGE_CURVE('',#2796,#2797,#1812,.T.);
#3398=EDGE_CURVE('',#2797,#2794,#1813,.T.);
#3399=EDGE_CURVE('',#2796,#2798,#1814,.T.);
#3400=EDGE_CURVE('',#2798,#2799,#1815,.T.);
#3401=EDGE_CURVE('',#2799,#2797,#1816,.T.);
#3402=EDGE_CURVE('',#2798,#2800,#1817,.T.);
#3403=EDGE_CURVE('',#2800,#2801,#1818,.T.);
#3404=EDGE_CURVE('',#2801,#2799,#1819,.T.);
#3405=EDGE_CURVE('',#2800,#2802,#1820,.T.);
#3406=EDGE_CURVE('',#2802,#2803,#1821,.T.);
#3407=EDGE_CURVE('',#2803,#2801,#1822,.T.);
#3408=EDGE_CURVE('',#2802,#2792,#1823,.T.);
#3409=EDGE_CURVE('',#2795,#2803,#1824,.T.);
#4558=ORIENTED_EDGE('',*,*,#3378,.F.);
#4559=ORIENTED_EDGE('',*,*,#3379,.F.);
#4560=ORIENTED_EDGE('',*,*,#3380,.T.);
#4561=ORIENTED_EDGE('',*,*,#3378,.T.);
#4562=ORIENTED_EDGE('',*,*,#3380,.F.);
#4563=ORIENTED_EDGE('',*,*,#3381,.F.);
#4564=ORIENTED_EDGE('',*,*,#3382,.T.);
#4565=ORIENTED_EDGE('',*,*,#3379,.T.);
#4566=ORIENTED_EDGE('',*,*,#3382,.F.);
#4567=ORIENTED_EDGE('',*,*,#3383,.F.);
#4568=ORIENTED_EDGE('',*,*,#3384,.T.);
#4569=ORIENTED_EDGE('',*,*,#3381,.T.);
#4570=ORIENTED_EDGE('',*,*,#3384,.F.);
#4571=ORIENTED_EDGE('',*,*,#3383,.T.);
#4572=ORIENTED_EDGE('',*,*,#3385,.F.);
#4573=ORIENTED_EDGE('',*,*,#3386,.F.);
#4574=ORIENTED_EDGE('',*,*,#3387,.T.);
#4575=ORIENTED_EDGE('',*,*,#3385,.T.);
#4576=ORIENTED_EDGE('',*,*,#3387,.F.);
#4577=ORIENTED_EDGE('',*,*,#3388,.F.);
#4578=ORIENTED_EDGE('',*,*,#3389,.T.);
#4579=ORIENTED_EDGE('',*,*,#3386,.T.);
#4580=ORIENTED_EDGE('',*,*,#3389,.F.);
#4581=ORIENTED_EDGE('',*,*,#3390,.F.);
#4582=ORIENTED_EDGE('',*,*,#3391,.T.);
#4583=ORIENTED_EDGE('',*,*,#3388,.T.);
#4584=ORIENTED_EDGE('',*,*,#3391,.F.);
#4585=ORIENTED_EDGE('',*,*,#3390,.T.);
#4586=ORIENTED_EDGE('',*,*,#3392,.T.);
#4587=ORIENTED_EDGE('',*,*,#3393,.T.);
#4588=ORIENTED_EDGE('',*,*,#3394,.T.);
#4589=ORIENTED_EDGE('',*,*,#3395,.F.);
#4590=ORIENTED_EDGE('',*,*,#3396,.T.);
#4591=ORIENTED_EDGE('',*,*,#3397,.T.);
#4592=ORIENTED_EDGE('',*,*,#3398,.T.);
#4593=ORIENTED_EDGE('',*,*,#3393,.F.);
#4594=ORIENTED_EDGE('',*,*,#3399,.T.);
#4595=ORIENTED_EDGE('',*,*,#3400,.T.);
#4596=ORIENTED_EDGE('',*,*,#3401,.T.);
#4597=ORIENTED_EDGE('',*,*,#3397,.F.);
#4598=ORIENTED_EDGE('',*,*,#3402,.T.);
#4599=ORIENTED_EDGE('',*,*,#3403,.T.);
#4600=ORIENTED_EDGE('',*,*,#3404,.T.);
#4601=ORIENTED_EDGE('',*,*,#3400,.F.);
#4602=ORIENTED_EDGE('',*,*,#3405,.T.);
#4603=ORIENTED_EDGE('',*,*,#3406,.T.);
#4604=ORIENTED_EDGE('',*,*,#3407,.T.);
#4605=ORIENTED_EDGE('',*,*,#3403,.F.);
#4606=ORIENTED_EDGE('',*,*,#3408,.T.);
#4607=ORIENTED_EDGE('',*,*,#3395,.T.);
#4608=ORIENTED_EDGE('',*,*,#3409,.T.);
#4609=ORIENTED_EDGE('',*,*,#3406,.F.);
#4610=ORIENTED_EDGE('',*,*,#3408,.F.);
#4611=ORIENTED_EDGE('',*,*,#3405,.F.);
#4612=ORIENTED_EDGE('',*,*,#3402,.F.);
#4613=ORIENTED_EDGE('',*,*,#3399,.F.);
#4614=ORIENTED_EDGE('',*,*,#3396,.F.);
#4615=ORIENTED_EDGE('',*,*,#3392,.F.);
#4616=ORIENTED_EDGE('',*,*,#3409,.F.);
#4617=ORIENTED_EDGE('',*,*,#3394,.F.);
#4618=ORIENTED_EDGE('',*,*,#3398,.F.);
#4619=ORIENTED_EDGE('',*,*,#3401,.F.);
#4620=ORIENTED_EDGE('',*,*,#3404,.F.);
#4621=ORIENTED_EDGE('',*,*,#3407,.F.);
#4729=CYLINDRICAL_SURFACE('',#6012,0.35);
#4730=CYLINDRICAL_SURFACE('',#6020,0.1954);
#5028=ADVANCED_FACE('',(#1033),#725,.T.);
#5029=ADVANCED_FACE('',(#1034),#34,.T.);
#5030=ADVANCED_FACE('',(#1035),#4729,.T.);
#5031=ADVANCED_FACE('',(#1036),#35,.T.);
#5032=ADVANCED_FACE('',(#1037,#544),#726,.T.);
#5033=ADVANCED_FACE('',(#1038),#36,.T.);
#5034=ADVANCED_FACE('',(#1039),#4730,.T.);
#5035=ADVANCED_FACE('',(#1040),#37,.T.);
#5036=ADVANCED_FACE('',(#1041),#727,.T.);
#5037=ADVANCED_FACE('',(#1042),#728,.F.);
#5038=ADVANCED_FACE('',(#1043),#729,.F.);
#5039=ADVANCED_FACE('',(#1044),#730,.F.);
#5040=ADVANCED_FACE('',(#1045),#731,.F.);
#5041=ADVANCED_FACE('',(#1046),#732,.F.);
#5042=ADVANCED_FACE('',(#1047),#733,.F.);
#5043=ADVANCED_FACE('',(#1048),#734,.F.);
#5044=ADVANCED_FACE('',(#1049),#735,.F.);
#5077=CLOSED_SHELL('',(#5028,#5029,#5030,#5031,#5032,#5033,#5034,#5035,
#5036));
#5078=CLOSED_SHELL('',(#5037,#5038,#5039,#5040,#5041,#5042,#5043,#5044));
#6007=AXIS2_PLACEMENT_3D('',#10064,#7550,#7551);
#6008=AXIS2_PLACEMENT_3D('',#10065,#7552,#7553);
#6009=AXIS2_PLACEMENT_3D('',#10067,#7554,#7555);
#6010=AXIS2_PLACEMENT_3D('',#10068,#7556,#7557);
#6011=AXIS2_PLACEMENT_3D('',#10070,#7558,#7559);
#6012=AXIS2_PLACEMENT_3D('',#10072,#7561,#7562);
#6013=AXIS2_PLACEMENT_3D('',#10074,#7563,#7564);
#6014=AXIS2_PLACEMENT_3D('',#10076,#7566,#7567);
#6015=AXIS2_PLACEMENT_3D('',#10078,#7568,#7569);
#6016=AXIS2_PLACEMENT_3D('',#10080,#7571,#7572);
#6017=AXIS2_PLACEMENT_3D('',#10082,#7573,#7574);
#6018=AXIS2_PLACEMENT_3D('',#10083,#7575,#7576);
#6019=AXIS2_PLACEMENT_3D('',#10085,#7577,#7578);
#6020=AXIS2_PLACEMENT_3D('',#10087,#7580,#7581);
#6021=AXIS2_PLACEMENT_3D('',#10089,#7582,#7583);
#6022=AXIS2_PLACEMENT_3D('',#10091,#7585,#7586);
#6023=AXIS2_PLACEMENT_3D('',#10093,#7587,#7588);
#6024=AXIS2_PLACEMENT_3D('',#10095,#7590,#7591);
#6025=AXIS2_PLACEMENT_3D('',#10096,#7592,#7593);
#6026=AXIS2_PLACEMENT_3D('',#10105,#7598,#7599);
#6027=AXIS2_PLACEMENT_3D('',#10111,#7603,#7604);
#6028=AXIS2_PLACEMENT_3D('',#10117,#7608,#7609);
#6029=AXIS2_PLACEMENT_3D('',#10123,#7613,#7614);
#6030=AXIS2_PLACEMENT_3D('',#10129,#7618,#7619);
#6031=AXIS2_PLACEMENT_3D('',#10132,#7622,#7623);
#6032=AXIS2_PLACEMENT_3D('',#10133,#7624,#7625);
#7550=DIRECTION('axis',(0.,0.,1.));
#7551=DIRECTION('refdir',(1.,0.,0.));
#7552=DIRECTION('center_axis',(0.,1.,0.));
#7553=DIRECTION('ref_axis',(0.,0.,1.));
#7554=DIRECTION('center_axis',(0.,-1.,0.));
#7555=DIRECTION('ref_axis',(1.,0.,0.));
#7556=DIRECTION('center_axis',(0.,-1.,0.));
#7557=DIRECTION('ref_axis',(1.,0.,0.));
#7558=DIRECTION('center_axis',(0.,-1.,0.));
#7559=DIRECTION('ref_axis',(1.,0.,0.));
#7560=DIRECTION('',(0.707106781186547,0.707106781186548,8.65956056235493E-17));
#7561=DIRECTION('center_axis',(0.,-1.,0.));
#7562=DIRECTION('ref_axis',(1.,0.,0.));
#7563=DIRECTION('center_axis',(0.,-1.,0.));
#7564=DIRECTION('ref_axis',(1.,0.,0.));
#7565=DIRECTION('',(0.,1.,0.));
#7566=DIRECTION('center_axis',(0.,1.,0.));
#7567=DIRECTION('ref_axis',(1.,0.,0.));
#7568=DIRECTION('center_axis',(0.,-1.,0.));
#7569=DIRECTION('ref_axis',(1.,0.,0.));
#7570=DIRECTION('',(-0.707106781186547,0.707106781186548,-8.65956056235493E-17));
#7571=DIRECTION('center_axis',(0.,-1.,0.));
#7572=DIRECTION('ref_axis',(0.,0.,-1.));
#7573=DIRECTION('center_axis',(0.,-1.,0.));
#7574=DIRECTION('ref_axis',(1.,0.,0.));
#7575=DIRECTION('center_axis',(0.,1.,0.));
#7576=DIRECTION('ref_axis',(1.,0.,0.));
#7577=DIRECTION('center_axis',(0.,1.,0.));
#7578=DIRECTION('ref_axis',(1.,0.,0.));
#7579=DIRECTION('',(-0.447213595499958,0.894427190999916,-5.47678698264203E-17));
#7580=DIRECTION('center_axis',(0.,-1.,0.));
#7581=DIRECTION('ref_axis',(1.,0.,0.));
#7582=DIRECTION('center_axis',(0.,1.,0.));
#7583=DIRECTION('ref_axis',(1.,0.,0.));
#7584=DIRECTION('',(0.,1.,0.));
#7585=DIRECTION('center_axis',(0.,1.,0.));
#7586=DIRECTION('ref_axis',(1.,0.,0.));
#7587=DIRECTION('center_axis',(0.,-1.,0.));
#7588=DIRECTION('ref_axis',(1.,0.,0.));
#7589=DIRECTION('',(-0.707106781186547,0.707106781186548,-8.65956056235493E-17));
#7590=DIRECTION('center_axis',(0.,-1.,0.));
#7591=DIRECTION('ref_axis',(0.,0.,-1.));
#7592=DIRECTION('center_axis',(0.866025403784439,0.,-0.5));
#7593=DIRECTION('ref_axis',(0.5,0.,0.866025403784439));
#7594=DIRECTION('',(-0.5,0.,-0.866025403784439));
#7595=DIRECTION('',(0.,-1.,0.));
#7596=DIRECTION('',(0.5,0.,0.866025403784439));
#7597=DIRECTION('',(0.,-1.,0.));
#7598=DIRECTION('center_axis',(1.60246890531964E-16,0.,-1.));
#7599=DIRECTION('ref_axis',(1.,0.,1.60246890531964E-16));
#7600=DIRECTION('',(-1.,0.,-1.60246890531964E-16));
#7601=DIRECTION('',(0.,-1.,0.));
#7602=DIRECTION('',(1.,0.,1.60246890531964E-16));
#7603=DIRECTION('center_axis',(-0.866025403784439,0.,-0.5));
#7604=DIRECTION('ref_axis',(0.5,0.,-0.866025403784439));
#7605=DIRECTION('',(-0.5,0.,0.866025403784439));
#7606=DIRECTION('',(0.,-1.,0.));
#7607=DIRECTION('',(0.5,0.,-0.866025403784439));
#7608=DIRECTION('center_axis',(-0.866025403784439,0.,0.5));
#7609=DIRECTION('ref_axis',(-0.5,0.,-0.866025403784439));
#7610=DIRECTION('',(0.5,0.,0.866025403784439));
#7611=DIRECTION('',(0.,-1.,0.));
#7612=DIRECTION('',(-0.5,0.,-0.866025403784439));
#7613=DIRECTION('center_axis',(-1.60246890531964E-16,0.,1.));
#7614=DIRECTION('ref_axis',(-1.,0.,-1.60246890531964E-16));
#7615=DIRECTION('',(1.,0.,1.60246890531964E-16));
#7616=DIRECTION('',(0.,-1.,0.));
#7617=DIRECTION('',(-1.,0.,-1.60246890531964E-16));
#7618=DIRECTION('center_axis',(0.866025403784439,0.,0.5));
#7619=DIRECTION('ref_axis',(-0.5,0.,0.866025403784439));
#7620=DIRECTION('',(0.5,0.,-0.866025403784439));
#7621=DIRECTION('',(-0.5,0.,0.866025403784439));
#7622=DIRECTION('center_axis',(0.,1.,0.));
#7623=DIRECTION('ref_axis',(1.,0.,0.));
#7624=DIRECTION('center_axis',(0.,-1.,0.));
#7625=DIRECTION('ref_axis',(0.,0.,-1.));
#10064=CARTESIAN_POINT('',(0.,0.,0.));
#10065=CARTESIAN_POINT('Origin',(0.3,0.4,0.));
#10066=CARTESIAN_POINT('',(-0.3,0.4,-3.67394039744206E-17));
#10067=CARTESIAN_POINT('Origin',(0.,0.4,0.));
#10068=CARTESIAN_POINT('Origin',(0.,0.375,0.));
#10069=CARTESIAN_POINT('',(-0.35,0.35,-4.28626379701573E-17));
#10070=CARTESIAN_POINT('Origin',(0.,0.35,0.));
#10071=CARTESIAN_POINT('',(-0.325,0.375,-3.9801020972289E-17));
#10072=CARTESIAN_POINT('Origin',(0.,0.19,0.));
#10073=CARTESIAN_POINT('',(-0.35,0.03,-4.28626379701574E-17));
#10074=CARTESIAN_POINT('Origin',(0.,0.03,0.));
#10075=CARTESIAN_POINT('',(-0.35,0.19,-4.28626379701574E-17));
#10076=CARTESIAN_POINT('Origin',(0.,0.0149999999999999,0.));
#10077=CARTESIAN_POINT('',(-0.32,-3.29597460435593E-17,-3.91886975727153E-17));
#10078=CARTESIAN_POINT('Origin',(0.,0.,0.));
#10079=CARTESIAN_POINT('',(-0.335,0.0149999999999999,-4.10256677714363E-17));
#10080=CARTESIAN_POINT('Origin',(0.22,0.,0.));
#10081=CARTESIAN_POINT('',(-0.22,-6.93889390390723E-18,-2.69422295812418E-17));
#10082=CARTESIAN_POINT('Origin',(0.,0.,0.));
#10083=CARTESIAN_POINT('Origin',(0.,-0.02,0.));
#10084=CARTESIAN_POINT('',(-0.1954,-0.0492,2.39295984553393E-17));
#10085=CARTESIAN_POINT('Origin',(0.,-0.0492,0.));
#10086=CARTESIAN_POINT('',(-0.21,-0.02,-2.57175827820944E-17));
#10087=CARTESIAN_POINT('Origin',(0.,-0.8,0.));
#10088=CARTESIAN_POINT('',(-0.1954,-1.5646,2.39295984553393E-17));
#10089=CARTESIAN_POINT('Origin',(0.,-1.5646,0.));
#10090=CARTESIAN_POINT('',(-0.1954,-0.8,-2.39295984553393E-17));
#10091=CARTESIAN_POINT('Origin',(0.,-1.58,0.));
#10092=CARTESIAN_POINT('',(-0.16,-1.6,-1.95943487863577E-17));
#10093=CARTESIAN_POINT('Origin',(0.,-1.6,0.));
#10094=CARTESIAN_POINT('',(-0.18,-1.58,-2.20436423846524E-17));
#10095=CARTESIAN_POINT('Origin',(0.,-1.6,0.));
#10096=CARTESIAN_POINT('Origin',(0.0866025403784439,-0.4,-0.15));
#10097=CARTESIAN_POINT('',(0.173205080756888,-0.4,0.));
#10098=CARTESIAN_POINT('',(0.0866025403784439,-0.4,-0.15));
#10099=CARTESIAN_POINT('',(0.173205080756888,-0.4,0.));
#10100=CARTESIAN_POINT('',(0.0866025403784439,-0.64,-0.15));
#10101=CARTESIAN_POINT('',(0.0866025403784439,-0.4,-0.15));
#10102=CARTESIAN_POINT('',(0.173205080756888,-0.64,0.));
#10103=CARTESIAN_POINT('',(0.173205080756888,-0.64,0.));
#10104=CARTESIAN_POINT('',(0.173205080756888,-0.4,0.));
#10105=CARTESIAN_POINT('Origin',(-0.0866025403784438,-0.4,-0.15));
#10106=CARTESIAN_POINT('',(-0.0866025403784438,-0.4,-0.15));
#10107=CARTESIAN_POINT('',(0.0866025403784439,-0.4,-0.15));
#10108=CARTESIAN_POINT('',(-0.0866025403784438,-0.64,-0.15));
#10109=CARTESIAN_POINT('',(-0.0866025403784438,-0.4,-0.15));
#10110=CARTESIAN_POINT('',(0.0866025403784439,-0.64,-0.15));
#10111=CARTESIAN_POINT('Origin',(-0.173205080756888,-0.4,-2.77555756156289E-17));
#10112=CARTESIAN_POINT('',(-0.173205080756888,-0.4,-2.12115047744981E-17));
#10113=CARTESIAN_POINT('',(-0.0866025403784438,-0.4,-0.15));
#10114=CARTESIAN_POINT('',(-0.173205080756888,-0.64,-2.77555756156289E-17));
#10115=CARTESIAN_POINT('',(-0.173205080756888,-0.4,-2.12115047744981E-17));
#10116=CARTESIAN_POINT('',(-0.0866025403784438,-0.64,-0.15));
#10117=CARTESIAN_POINT('Origin',(-0.0866025403784439,-0.4,0.15));
#10118=CARTESIAN_POINT('',(-0.0866025403784439,-0.4,0.15));
#10119=CARTESIAN_POINT('',(-0.173205080756888,-0.4,-2.12115047744981E-17));
#10120=CARTESIAN_POINT('',(-0.0866025403784439,-0.64,0.15));
#10121=CARTESIAN_POINT('',(-0.0866025403784439,-0.4,0.15));
#10122=CARTESIAN_POINT('',(-0.173205080756888,-0.64,-2.12115047744981E-17));
#10123=CARTESIAN_POINT('Origin',(0.0866025403784439,-0.4,0.15));
#10124=CARTESIAN_POINT('',(0.0866025403784439,-0.4,0.15));
#10125=CARTESIAN_POINT('',(-0.0866025403784439,-0.4,0.15));
#10126=CARTESIAN_POINT('',(0.0866025403784439,-0.64,0.15));
#10127=CARTESIAN_POINT('',(0.0866025403784439,-0.4,0.15));
#10128=CARTESIAN_POINT('',(-0.0866025403784439,-0.64,0.15));
#10129=CARTESIAN_POINT('Origin',(0.173205080756888,-0.4,0.));
#10130=CARTESIAN_POINT('',(0.0866025403784439,-0.4,0.15));
#10131=CARTESIAN_POINT('',(0.0866025403784439,-0.64,0.15));
#10132=CARTESIAN_POINT('Origin',(0.,-0.4,-2.77555756156289E-17));
#10133=CARTESIAN_POINT('Origin',(0.,-0.64,-2.77555756156289E-17));
#10226=UNCERTAINTY_MEASURE_WITH_UNIT(LENGTH_MEASURE(0.001),#10266,
'DISTANCE_ACCURACY_VALUE',
'Maximum model space distance between geometric entities at asserted c
onnectivities');
#10227=UNCERTAINTY_MEASURE_WITH_UNIT(LENGTH_MEASURE(0.001),#10266,
'DISTANCE_ACCURACY_VALUE',
'Maximum model space distance between geometric entities at asserted c
onnectivities');
#10264=(
GEOMETRIC_REPRESENTATION_CONTEXT(3)
GLOBAL_UNCERTAINTY_ASSIGNED_CONTEXT((#10226))
GLOBAL_UNIT_ASSIGNED_CONTEXT((#10266,#10268,#10269))
REPRESENTATION_CONTEXT('','3D')
);
#10265=(
GEOMETRIC_REPRESENTATION_CONTEXT(3)
GLOBAL_UNCERTAINTY_ASSIGNED_CONTEXT((#10227))
GLOBAL_UNIT_ASSIGNED_CONTEXT((#10266,#10268,#10269))
REPRESENTATION_CONTEXT('','3D')
);
#10266=(
LENGTH_UNIT()
NAMED_UNIT(*)
SI_UNIT(.CENTI.,.METRE.)
);
#10268=(
NAMED_UNIT(*)
PLANE_ANGLE_UNIT()
SI_UNIT($,.RADIAN.)
);
#10269=(
NAMED_UNIT(*)
SI_UNIT($,.STERADIAN.)
SOLID_ANGLE_UNIT()
);
#10306=SHAPE_DEFINITION_REPRESENTATION(#10347,#10440);
#10347=PRODUCT_DEFINITION_SHAPE('',$,#10478);
#10440=SHAPE_REPRESENTATION('',(#6007),#10264);
#10441=PRODUCT_DEFINITION_CONTEXT('part definition',#10554,'design');
#10478=PRODUCT_DEFINITION('Cap Screw - M4x16','Cap Screw - M4x16',#10515,
#10441);
#10515=PRODUCT_DEFINITION_FORMATION('',$,#10592);
#10554=APPLICATION_CONTEXT(
'Core Data for Automotive Mechanical Design Process');
#10555=PRODUCT_CONTEXT('part definition',#10554,'mechanical');
#10592=PRODUCT('Cap Screw - M4x16','Cap Screw - M4x16',
'Cap Screw - M4x16',(#10555));
#10656=COLOUR_RGB('Black',0.12,0.14,0.17);
#10657=FILL_AREA_STYLE_COLOUR('',#10656);
#10658=FILL_AREA_STYLE('',(#10657));
#10659=SURFACE_STYLE_FILL_AREA(#10658);
#10660=SURFACE_SIDE_STYLE('',(#10659));
#10661=SURFACE_STYLE_USAGE(.BOTH.,#10660);
#10662=PRESENTATION_STYLE_ASSIGNMENT((#10661));
ENDSEC;
END-ISO-10303-21;
